ISO-10303-21;
HEADER;
/* Generated by software containing ST-Developer
 * from STEP Tools, Inc. (www.steptools.com) 
 */
/* OPTION: using custom renumber hook */

FILE_DESCRIPTION(
/* description */ ('STEP AP242 Edition 2', 'CAx-IF Rec.Pracs.---Representation and Presentation of Product Manufa
cturing Information (PMI)---4.0---2014-10-13', 'CAx-IF Rec.Pracs.---3D Tessellated Geometry---0.4---2014-09-14', '2;1', 'CAx-IF Rec.Pracs.---User Defined Attributes---1.5---2016-08-15'),
/* implementation_level */ '2;1');

FILE_NAME(
/* name */ 'Floating_ring.step',
/* time_stamp */ '2026-10-08T12:15:07Z',
/* author */ (''),
/* organization */ (''),
/* preprocessor_version */ 'ST-DEVELOPER v20',
/* originating_system */ 'ONSHAPE BY PTC INC, 1.221',
/* authorisation */ '  ');

FILE_SCHEMA (('AP242_MANAGED_MODEL_BASED_3D_ENGINEERING_MIM_LF { 1 0 10303 442 3 1 4 }'));
ENDSEC;

DATA;
#60=COLOUR_RGB('', 0.66274510, 0.83137255, 0.94901961);
#217=SHAPE_REPRESENTATION_RELATIONSHIP('','',#13791,#244);
#244=ADVANCED_BREP_SHAPE_REPRESENTATION('',(#13735),#45481);
#317=TOROIDAL_SURFACE('',#14756,0.0104331778036387,0.001);
#318=TOROIDAL_SURFACE('',#14757,0.044,0.001);
#319=TOROIDAL_SURFACE('',#14758,0.044,0.001);
#320=TOROIDAL_SURFACE('',#14759,0.0104331778036387,0.001);
#775=CIRCLE('',#14701,0.001);
#776=CIRCLE('',#14702,0.001);
#777=CIRCLE('',#14707,0.001);
#778=CIRCLE('',#14708,0.001);
#779=CIRCLE('',#14712,0.001);
#780=CIRCLE('',#14713,0.001);
#781=CIRCLE('',#14715,0.00277876);
#782=CIRCLE('',#14716,0.0012192);
#783=CIRCLE('',#14718,0.00277876);
#784=CIRCLE('',#14719,0.0012192);
#785=CIRCLE('',#14721,0.00277876);
#786=CIRCLE('',#14722,0.0012192);
#787=CIRCLE('',#14724,0.00277876);
#788=CIRCLE('',#14725,0.00277876);
#789=CIRCLE('',#14726,0.00277876);
#790=CIRCLE('',#14727,0.001);
#791=CIRCLE('',#14728,0.001);
#792=CIRCLE('',#14729,0.001);
#793=CIRCLE('',#14730,0.0104331778036387);
#794=CIRCLE('',#14731,0.044);
#795=CIRCLE('',#14733,0.0012192);
#796=CIRCLE('',#14734,0.0012192);
#797=CIRCLE('',#14735,0.0012192);
#798=CIRCLE('',#14736,0.001);
#799=CIRCLE('',#14737,0.001);
#800=CIRCLE('',#14738,0.001);
#801=CIRCLE('',#14739,0.044);
#802=CIRCLE('',#14740,0.0104331778036387);
#803=CIRCLE('',#14742,0.045);
#804=CIRCLE('',#14743,0.045);
#805=CIRCLE('',#14745,0.00943317780363869);
#806=CIRCLE('',#14746,0.00943317780363869);
#1401=PLANE('',#14699);
#1402=PLANE('',#14703);
#1403=PLANE('',#14704);
#1404=PLANE('',#14705);
#1405=PLANE('',#14709);
#1406=PLANE('',#14710);
#1407=PLANE('',#14714);
#1408=PLANE('',#14717);
#1409=PLANE('',#14720);
#1410=PLANE('',#14723);
#1411=PLANE('',#14732);
#1703=CYLINDRICAL_SURFACE('',#14700,0.001);
#1704=CYLINDRICAL_SURFACE('',#14706,0.001);
#1705=CYLINDRICAL_SURFACE('',#14711,0.001);
#1706=CYLINDRICAL_SURFACE('',#14741,0.045);
#1707=CYLINDRICAL_SURFACE('',#14744,0.00943317780363869);
#1708=CYLINDRICAL_SURFACE('',#14747,0.0012192);
#1709=CYLINDRICAL_SURFACE('',#14748,0.00277876);
#1710=CYLINDRICAL_SURFACE('',#14749,0.0012192);
#1711=CYLINDRICAL_SURFACE('',#14750,0.00277876);
#1712=CYLINDRICAL_SURFACE('',#14751,0.0012192);
#1713=CYLINDRICAL_SURFACE('',#14752,0.00277876);
#1714=CYLINDRICAL_SURFACE('',#14753,0.001);
#1715=CYLINDRICAL_SURFACE('',#14754,0.001);
#1716=CYLINDRICAL_SURFACE('',#14755,0.001);
#4072=ORIENTED_EDGE('',*,*,#6683,.T.);
#4073=ORIENTED_EDGE('',*,*,#6684,.T.);
#4074=ORIENTED_EDGE('',*,*,#6685,.F.);
#4075=ORIENTED_EDGE('',*,*,#6686,.F.);
#4076=ORIENTED_EDGE('',*,*,#6685,.T.);
#4077=ORIENTED_EDGE('',*,*,#6687,.T.);
#4078=ORIENTED_EDGE('',*,*,#6688,.F.);
#4079=ORIENTED_EDGE('',*,*,#6689,.F.);
#4080=ORIENTED_EDGE('',*,*,#6688,.T.);
#4081=ORIENTED_EDGE('',*,*,#6690,.T.);
#4082=ORIENTED_EDGE('',*,*,#6691,.F.);
#4083=ORIENTED_EDGE('',*,*,#6692,.F.);
#4084=ORIENTED_EDGE('',*,*,#6693,.T.);
#4085=ORIENTED_EDGE('',*,*,#6694,.T.);
#4086=ORIENTED_EDGE('',*,*,#6695,.F.);
#4087=ORIENTED_EDGE('',*,*,#6696,.F.);
#4088=ORIENTED_EDGE('',*,*,#6697,.T.);
#4089=ORIENTED_EDGE('',*,*,#6698,.T.);
#4090=ORIENTED_EDGE('',*,*,#6699,.F.);
#4091=ORIENTED_EDGE('',*,*,#6700,.F.);
#4092=ORIENTED_EDGE('',*,*,#6699,.T.);
#4093=ORIENTED_EDGE('',*,*,#6701,.T.);
#4094=ORIENTED_EDGE('',*,*,#6693,.F.);
#4095=ORIENTED_EDGE('',*,*,#6702,.F.);
#4096=ORIENTED_EDGE('',*,*,#6703,.T.);
#4097=ORIENTED_EDGE('',*,*,#6704,.T.);
#4098=ORIENTED_EDGE('',*,*,#6705,.F.);
#4099=ORIENTED_EDGE('',*,*,#6706,.F.);
#4100=ORIENTED_EDGE('',*,*,#6707,.T.);
#4101=ORIENTED_EDGE('',*,*,#6708,.T.);
#4102=ORIENTED_EDGE('',*,*,#6709,.F.);
#4103=ORIENTED_EDGE('',*,*,#6710,.F.);
#4104=ORIENTED_EDGE('',*,*,#6709,.T.);
#4105=ORIENTED_EDGE('',*,*,#6711,.T.);
#4106=ORIENTED_EDGE('',*,*,#6703,.F.);
#4107=ORIENTED_EDGE('',*,*,#6712,.F.);
#4108=ORIENTED_EDGE('',*,*,#6713,.T.);
#4109=ORIENTED_EDGE('',*,*,#6714,.F.);
#4110=ORIENTED_EDGE('',*,*,#6715,.T.);
#4111=ORIENTED_EDGE('',*,*,#6716,.F.);
#4112=ORIENTED_EDGE('',*,*,#6717,.T.);
#4113=ORIENTED_EDGE('',*,*,#6718,.F.);
#4114=ORIENTED_EDGE('',*,*,#6719,.F.);
#4115=ORIENTED_EDGE('',*,*,#6720,.F.);
#4116=ORIENTED_EDGE('',*,*,#6721,.F.);
#4117=ORIENTED_EDGE('',*,*,#6711,.F.);
#4118=ORIENTED_EDGE('',*,*,#6708,.F.);
#4119=ORIENTED_EDGE('',*,*,#6722,.F.);
#4120=ORIENTED_EDGE('',*,*,#6704,.F.);
#4121=ORIENTED_EDGE('',*,*,#6701,.F.);
#4122=ORIENTED_EDGE('',*,*,#6698,.F.);
#4123=ORIENTED_EDGE('',*,*,#6723,.F.);
#4124=ORIENTED_EDGE('',*,*,#6694,.F.);
#4125=ORIENTED_EDGE('',*,*,#6724,.F.);
#4126=ORIENTED_EDGE('',*,*,#6690,.F.);
#4127=ORIENTED_EDGE('',*,*,#6687,.F.);
#4128=ORIENTED_EDGE('',*,*,#6684,.F.);
#4129=ORIENTED_EDGE('',*,*,#6725,.T.);
#4130=ORIENTED_EDGE('',*,*,#6726,.T.);
#4131=ORIENTED_EDGE('',*,*,#6727,.T.);
#4132=ORIENTED_EDGE('',*,*,#6728,.T.);
#4133=ORIENTED_EDGE('',*,*,#6729,.T.);
#4134=ORIENTED_EDGE('',*,*,#6710,.T.);
#4135=ORIENTED_EDGE('',*,*,#6712,.T.);
#4136=ORIENTED_EDGE('',*,*,#6706,.T.);
#4137=ORIENTED_EDGE('',*,*,#6730,.T.);
#4138=ORIENTED_EDGE('',*,*,#6700,.T.);
#4139=ORIENTED_EDGE('',*,*,#6702,.T.);
#4140=ORIENTED_EDGE('',*,*,#6696,.T.);
#4141=ORIENTED_EDGE('',*,*,#6731,.T.);
#4142=ORIENTED_EDGE('',*,*,#6692,.T.);
#4143=ORIENTED_EDGE('',*,*,#6732,.T.);
#4144=ORIENTED_EDGE('',*,*,#6686,.T.);
#4145=ORIENTED_EDGE('',*,*,#6689,.T.);
#4146=ORIENTED_EDGE('',*,*,#6733,.T.);
#4147=ORIENTED_EDGE('',*,*,#6734,.T.);
#4148=ORIENTED_EDGE('',*,*,#6735,.T.);
#4149=ORIENTED_EDGE('',*,*,#6736,.T.);
#4150=ORIENTED_EDGE('',*,*,#6737,.T.);
#4151=ORIENTED_EDGE('',*,*,#6738,.T.);
#4152=ORIENTED_EDGE('',*,*,#6718,.T.);
#4153=ORIENTED_EDGE('',*,*,#6727,.F.);
#4154=ORIENTED_EDGE('',*,*,#6719,.T.);
#4155=ORIENTED_EDGE('',*,*,#6717,.F.);
#4156=ORIENTED_EDGE('',*,*,#6716,.T.);
#4157=ORIENTED_EDGE('',*,*,#6728,.F.);
#4158=ORIENTED_EDGE('',*,*,#6720,.T.);
#4159=ORIENTED_EDGE('',*,*,#6715,.F.);
#4160=ORIENTED_EDGE('',*,*,#6714,.T.);
#4161=ORIENTED_EDGE('',*,*,#6729,.F.);
#4162=ORIENTED_EDGE('',*,*,#6721,.T.);
#4163=ORIENTED_EDGE('',*,*,#6713,.F.);
#4164=ORIENTED_EDGE('',*,*,#6730,.F.);
#4165=ORIENTED_EDGE('',*,*,#6705,.T.);
#4166=ORIENTED_EDGE('',*,*,#6722,.T.);
#4167=ORIENTED_EDGE('',*,*,#6707,.F.);
#4168=ORIENTED_EDGE('',*,*,#6731,.F.);
#4169=ORIENTED_EDGE('',*,*,#6695,.T.);
#4170=ORIENTED_EDGE('',*,*,#6723,.T.);
#4171=ORIENTED_EDGE('',*,*,#6697,.F.);
#4172=ORIENTED_EDGE('',*,*,#6732,.F.);
#4173=ORIENTED_EDGE('',*,*,#6691,.T.);
#4174=ORIENTED_EDGE('',*,*,#6724,.T.);
#4175=ORIENTED_EDGE('',*,*,#6683,.F.);
#4176=ORIENTED_EDGE('',*,*,#6734,.F.);
#4177=ORIENTED_EDGE('',*,*,#6738,.F.);
#4178=ORIENTED_EDGE('',*,*,#6736,.F.);
#4179=ORIENTED_EDGE('',*,*,#6733,.F.);
#4180=ORIENTED_EDGE('',*,*,#6726,.F.);
#4181=ORIENTED_EDGE('',*,*,#6735,.F.);
#4182=ORIENTED_EDGE('',*,*,#6737,.F.);
#4183=ORIENTED_EDGE('',*,*,#6725,.F.);
#6683=EDGE_CURVE('',#8213,#8214,#9255,.T.);
#6684=EDGE_CURVE('',#8214,#8215,#9256,.T.);
#6685=EDGE_CURVE('',#8216,#8215,#9257,.T.);
#6686=EDGE_CURVE('',#8213,#8216,#9258,.T.);
#6687=EDGE_CURVE('',#8215,#8217,#775,.T.);
#6688=EDGE_CURVE('',#8218,#8217,#9259,.T.);
#6689=EDGE_CURVE('',#8216,#8218,#776,.T.);
#6690=EDGE_CURVE('',#8217,#8219,#9260,.T.);
#6691=EDGE_CURVE('',#8220,#8219,#9261,.T.);
#6692=EDGE_CURVE('',#8218,#8220,#9262,.T.);
#6693=EDGE_CURVE('',#8221,#8222,#9263,.T.);
#6694=EDGE_CURVE('',#8222,#8223,#9264,.T.);
#6695=EDGE_CURVE('',#8224,#8223,#9265,.T.);
#6696=EDGE_CURVE('',#8221,#8224,#9266,.T.);
#6697=EDGE_CURVE('',#8225,#8226,#9267,.T.);
#6698=EDGE_CURVE('',#8226,#8227,#9268,.T.);
#6699=EDGE_CURVE('',#8228,#8227,#9269,.T.);
#6700=EDGE_CURVE('',#8225,#8228,#9270,.T.);
#6701=EDGE_CURVE('',#8227,#8222,#777,.T.);
#6702=EDGE_CURVE('',#8228,#8221,#778,.T.);
#6703=EDGE_CURVE('',#8229,#8230,#9271,.T.);
#6704=EDGE_CURVE('',#8230,#8231,#9272,.T.);
#6705=EDGE_CURVE('',#8232,#8231,#9273,.T.);
#6706=EDGE_CURVE('',#8229,#8232,#9274,.T.);
#6707=EDGE_CURVE('',#8233,#8234,#9275,.T.);
#6708=EDGE_CURVE('',#8234,#8235,#9276,.T.);
#6709=EDGE_CURVE('',#8236,#8235,#9277,.T.);
#6710=EDGE_CURVE('',#8233,#8236,#9278,.T.);
#6711=EDGE_CURVE('',#8235,#8230,#779,.T.);
#6712=EDGE_CURVE('',#8236,#8229,#780,.T.);
#6713=EDGE_CURVE('',#8237,#8237,#781,.T.);
#6714=EDGE_CURVE('',#8238,#8238,#782,.T.);
#6715=EDGE_CURVE('',#8239,#8239,#783,.T.);
#6716=EDGE_CURVE('',#8240,#8240,#784,.T.);
#6717=EDGE_CURVE('',#8241,#8241,#785,.T.);
#6718=EDGE_CURVE('',#8242,#8242,#786,.T.);
#6719=EDGE_CURVE('',#8243,#8243,#787,.T.);
#6720=EDGE_CURVE('',#8244,#8244,#788,.T.);
#6721=EDGE_CURVE('',#8245,#8245,#789,.T.);
#6722=EDGE_CURVE('',#8231,#8234,#790,.T.);
#6723=EDGE_CURVE('',#8223,#8226,#791,.T.);
#6724=EDGE_CURVE('',#8219,#8214,#792,.T.);
#6725=EDGE_CURVE('',#8246,#8246,#793,.T.);
#6726=EDGE_CURVE('',#8247,#8247,#794,.T.);
#6727=EDGE_CURVE('',#8248,#8248,#795,.T.);
#6728=EDGE_CURVE('',#8249,#8249,#796,.T.);
#6729=EDGE_CURVE('',#8250,#8250,#797,.T.);
#6730=EDGE_CURVE('',#8232,#8233,#798,.T.);
#6731=EDGE_CURVE('',#8224,#8225,#799,.T.);
#6732=EDGE_CURVE('',#8220,#8213,#800,.T.);
#6733=EDGE_CURVE('',#8251,#8251,#801,.T.);
#6734=EDGE_CURVE('',#8252,#8252,#802,.T.);
#6735=EDGE_CURVE('',#8253,#8253,#803,.T.);
#6736=EDGE_CURVE('',#8254,#8254,#804,.T.);
#6737=EDGE_CURVE('',#8255,#8255,#805,.T.);
#6738=EDGE_CURVE('',#8256,#8256,#806,.T.);
#8213=VERTEX_POINT('',#35052);
#8214=VERTEX_POINT('',#35053);
#8215=VERTEX_POINT('',#35055);
#8216=VERTEX_POINT('',#35057);
#8217=VERTEX_POINT('',#35061);
#8218=VERTEX_POINT('',#35063);
#8219=VERTEX_POINT('',#35067);
#8220=VERTEX_POINT('',#35069);
#8221=VERTEX_POINT('',#35073);
#8222=VERTEX_POINT('',#35074);
#8223=VERTEX_POINT('',#35076);
#8224=VERTEX_POINT('',#35078);
#8225=VERTEX_POINT('',#35082);
#8226=VERTEX_POINT('',#35083);
#8227=VERTEX_POINT('',#35085);
#8228=VERTEX_POINT('',#35087);
#8229=VERTEX_POINT('',#35094);
#8230=VERTEX_POINT('',#35095);
#8231=VERTEX_POINT('',#35097);
#8232=VERTEX_POINT('',#35099);
#8233=VERTEX_POINT('',#35103);
#8234=VERTEX_POINT('',#35104);
#8235=VERTEX_POINT('',#35106);
#8236=VERTEX_POINT('',#35108);
#8237=VERTEX_POINT('',#35115);
#8238=VERTEX_POINT('',#35117);
#8239=VERTEX_POINT('',#35120);
#8240=VERTEX_POINT('',#35122);
#8241=VERTEX_POINT('',#35125);
#8242=VERTEX_POINT('',#35127);
#8243=VERTEX_POINT('',#35130);
#8244=VERTEX_POINT('',#35132);
#8245=VERTEX_POINT('',#35134);
#8246=VERTEX_POINT('',#35139);
#8247=VERTEX_POINT('',#35141);
#8248=VERTEX_POINT('',#35144);
#8249=VERTEX_POINT('',#35146);
#8250=VERTEX_POINT('',#35148);
#8251=VERTEX_POINT('',#35153);
#8252=VERTEX_POINT('',#35155);
#8253=VERTEX_POINT('',#35158);
#8254=VERTEX_POINT('',#35160);
#8255=VERTEX_POINT('',#35163);
#8256=VERTEX_POINT('',#35165);
#9255=LINE('',#35051,#10083);
#9256=LINE('',#35054,#10084);
#9257=LINE('',#35056,#10085);
#9258=LINE('',#35058,#10086);
#9259=LINE('',#35062,#10087);
#9260=LINE('',#35066,#10088);
#9261=LINE('',#35068,#10089);
#9262=LINE('',#35070,#10090);
#9263=LINE('',#35072,#10091);
#9264=LINE('',#35075,#10092);
#9265=LINE('',#35077,#10093);
#9266=LINE('',#35079,#10094);
#9267=LINE('',#35081,#10095);
#9268=LINE('',#35084,#10096);
#9269=LINE('',#35086,#10097);
#9270=LINE('',#35088,#10098);
#9271=LINE('',#35093,#10099);
#9272=LINE('',#35096,#10100);
#9273=LINE('',#35098,#10101);
#9274=LINE('',#35100,#10102);
#9275=LINE('',#35102,#10103);
#9276=LINE('',#35105,#10104);
#9277=LINE('',#35107,#10105);
#9278=LINE('',#35109,#10106);
#10083=VECTOR('',#17573,1.);
#10084=VECTOR('',#17574,1.);
#10085=VECTOR('',#17575,1.);
#10086=VECTOR('',#17576,1.);
#10087=VECTOR('',#17581,1.);
#10088=VECTOR('',#17586,1.);
#10089=VECTOR('',#17587,1.);
#10090=VECTOR('',#17588,1.);
#10091=VECTOR('',#17591,1.);
#10092=VECTOR('',#17592,1.);
#10093=VECTOR('',#17593,1.);
#10094=VECTOR('',#17594,1.);
#10095=VECTOR('',#17597,1.);
#10096=VECTOR('',#17598,1.);
#10097=VECTOR('',#17599,1.);
#10098=VECTOR('',#17600,1.);
#10099=VECTOR('',#17609,1.);
#10100=VECTOR('',#17610,1.);
#10101=VECTOR('',#17611,1.);
#10102=VECTOR('',#17612,1.);
#10103=VECTOR('',#17615,1.);
#10104=VECTOR('',#17616,1.);
#10105=VECTOR('',#17617,1.);
#10106=VECTOR('',#17618,1.);
#11092=EDGE_LOOP('',(#4072,#4073,#4074,#4075));
#11093=EDGE_LOOP('',(#4076,#4077,#4078,#4079));
#11094=EDGE_LOOP('',(#4080,#4081,#4082,#4083));
#11095=EDGE_LOOP('',(#4084,#4085,#4086,#4087));
#11096=EDGE_LOOP('',(#4088,#4089,#4090,#4091));
#11097=EDGE_LOOP('',(#4092,#4093,#4094,#4095));
#11098=EDGE_LOOP('',(#4096,#4097,#4098,#4099));
#11099=EDGE_LOOP('',(#4100,#4101,#4102,#4103));
#11100=EDGE_LOOP('',(#4104,#4105,#4106,#4107));
#11101=EDGE_LOOP('',(#4108));
#11102=EDGE_LOOP('',(#4109));
#11103=EDGE_LOOP('',(#4110));
#11104=EDGE_LOOP('',(#4111));
#11105=EDGE_LOOP('',(#4112));
#11106=EDGE_LOOP('',(#4113));
#11107=EDGE_LOOP('',(#4114));
#11108=EDGE_LOOP('',(#4115));
#11109=EDGE_LOOP('',(#4116));
#11110=EDGE_LOOP('',(#4117,#4118,#4119,#4120));
#11111=EDGE_LOOP('',(#4121,#4122,#4123,#4124));
#11112=EDGE_LOOP('',(#4125,#4126,#4127,#4128));
#11113=EDGE_LOOP('',(#4129));
#11114=EDGE_LOOP('',(#4130));
#11115=EDGE_LOOP('',(#4131));
#11116=EDGE_LOOP('',(#4132));
#11117=EDGE_LOOP('',(#4133));
#11118=EDGE_LOOP('',(#4134,#4135,#4136,#4137));
#11119=EDGE_LOOP('',(#4138,#4139,#4140,#4141));
#11120=EDGE_LOOP('',(#4142,#4143,#4144,#4145));
#11121=EDGE_LOOP('',(#4146));
#11122=EDGE_LOOP('',(#4147));
#11123=EDGE_LOOP('',(#4148));
#11124=EDGE_LOOP('',(#4149));
#11125=EDGE_LOOP('',(#4150));
#11126=EDGE_LOOP('',(#4151));
#11127=EDGE_LOOP('',(#4152));
#11128=EDGE_LOOP('',(#4153));
#11129=EDGE_LOOP('',(#4154));
#11130=EDGE_LOOP('',(#4155));
#11131=EDGE_LOOP('',(#4156));
#11132=EDGE_LOOP('',(#4157));
#11133=EDGE_LOOP('',(#4158));
#11134=EDGE_LOOP('',(#4159));
#11135=EDGE_LOOP('',(#4160));
#11136=EDGE_LOOP('',(#4161));
#11137=EDGE_LOOP('',(#4162));
#11138=EDGE_LOOP('',(#4163));
#11139=EDGE_LOOP('',(#4164,#4165,#4166,#4167));
#11140=EDGE_LOOP('',(#4168,#4169,#4170,#4171));
#11141=EDGE_LOOP('',(#4172,#4173,#4174,#4175));
#11142=EDGE_LOOP('',(#4176));
#11143=EDGE_LOOP('',(#4177));
#11144=EDGE_LOOP('',(#4178));
#11145=EDGE_LOOP('',(#4179));
#11146=EDGE_LOOP('',(#4180));
#11147=EDGE_LOOP('',(#4181));
#11148=EDGE_LOOP('',(#4182));
#11149=EDGE_LOOP('',(#4183));
#12210=FACE_BOUND('',#11092,.T.);
#12211=FACE_BOUND('',#11093,.T.);
#12212=FACE_BOUND('',#11094,.T.);
#12213=FACE_BOUND('',#11095,.T.);
#12214=FACE_BOUND('',#11096,.T.);
#12215=FACE_BOUND('',#11097,.T.);
#12216=FACE_BOUND('',#11098,.T.);
#12217=FACE_BOUND('',#11099,.T.);
#12218=FACE_BOUND('',#11100,.T.);
#12219=FACE_BOUND('',#11101,.T.);
#12220=FACE_BOUND('',#11102,.T.);
#12221=FACE_BOUND('',#11103,.T.);
#12222=FACE_BOUND('',#11104,.T.);
#12223=FACE_BOUND('',#11105,.T.);
#12224=FACE_BOUND('',#11106,.T.);
#12225=FACE_BOUND('',#11107,.T.);
#12226=FACE_BOUND('',#11108,.T.);
#12227=FACE_BOUND('',#11109,.T.);
#12228=FACE_BOUND('',#11110,.T.);
#12229=FACE_BOUND('',#11111,.T.);
#12230=FACE_BOUND('',#11112,.T.);
#12231=FACE_BOUND('',#11113,.T.);
#12232=FACE_BOUND('',#11114,.T.);
#12233=FACE_BOUND('',#11115,.T.);
#12234=FACE_BOUND('',#11116,.T.);
#12235=FACE_BOUND('',#11117,.T.);
#12236=FACE_BOUND('',#11118,.T.);
#12237=FACE_BOUND('',#11119,.T.);
#12238=FACE_BOUND('',#11120,.T.);
#12239=FACE_BOUND('',#11121,.T.);
#12240=FACE_BOUND('',#11122,.T.);
#12241=FACE_BOUND('',#11123,.T.);
#12242=FACE_BOUND('',#11124,.T.);
#12243=FACE_BOUND('',#11125,.T.);
#12244=FACE_BOUND('',#11126,.T.);
#12245=FACE_BOUND('',#11127,.T.);
#12246=FACE_BOUND('',#11128,.T.);
#12247=FACE_BOUND('',#11129,.T.);
#12248=FACE_BOUND('',#11130,.T.);
#12249=FACE_BOUND('',#11131,.T.);
#12250=FACE_BOUND('',#11132,.T.);
#12251=FACE_BOUND('',#11133,.T.);
#12252=FACE_BOUND('',#11134,.T.);
#12253=FACE_BOUND('',#11135,.T.);
#12254=FACE_BOUND('',#11136,.T.);
#12255=FACE_BOUND('',#11137,.T.);
#12256=FACE_BOUND('',#11138,.T.);
#12257=FACE_BOUND('',#11139,.T.);
#12258=FACE_BOUND('',#11140,.T.);
#12259=FACE_BOUND('',#11141,.T.);
#12260=FACE_BOUND('',#11142,.T.);
#12261=FACE_BOUND('',#11143,.T.);
#12262=FACE_BOUND('',#11144,.T.);
#12263=FACE_BOUND('',#11145,.T.);
#12264=FACE_BOUND('',#11146,.T.);
#12265=FACE_BOUND('',#11147,.T.);
#12266=FACE_BOUND('',#11148,.T.);
#12267=FACE_BOUND('',#11149,.T.);
#13183=ADVANCED_FACE('',(#12210),#1401,.F.);
#13184=ADVANCED_FACE('',(#12211),#1703,.F.);
#13185=ADVANCED_FACE('',(#12212),#1402,.F.);
#13186=ADVANCED_FACE('',(#12213),#1403,.F.);
#13187=ADVANCED_FACE('',(#12214),#1404,.F.);
#13188=ADVANCED_FACE('',(#12215),#1704,.F.);
#13189=ADVANCED_FACE('',(#12216),#1405,.F.);
#13190=ADVANCED_FACE('',(#12217),#1406,.F.);
#13191=ADVANCED_FACE('',(#12218),#1705,.F.);
#13192=ADVANCED_FACE('',(#12219,#12220),#1407,.F.);
#13193=ADVANCED_FACE('',(#12221,#12222),#1408,.F.);
#13194=ADVANCED_FACE('',(#12223,#12224),#1409,.F.);
#13195=ADVANCED_FACE('',(#12225,#12226,#12227,#12228,#12229,#12230,#12231,
#12232),#1410,.T.);
#13196=ADVANCED_FACE('',(#12233,#12234,#12235,#12236,#12237,#12238,#12239,
#12240),#1411,.F.);
#13197=ADVANCED_FACE('',(#12241,#12242),#1706,.T.);
#13198=ADVANCED_FACE('',(#12243,#12244),#1707,.F.);
#13199=ADVANCED_FACE('',(#12245,#12246),#1708,.F.);
#13200=ADVANCED_FACE('',(#12247,#12248),#1709,.F.);
#13201=ADVANCED_FACE('',(#12249,#12250),#1710,.F.);
#13202=ADVANCED_FACE('',(#12251,#12252),#1711,.F.);
#13203=ADVANCED_FACE('',(#12253,#12254),#1712,.F.);
#13204=ADVANCED_FACE('',(#12255,#12256),#1713,.F.);
#13205=ADVANCED_FACE('',(#12257),#1714,.F.);
#13206=ADVANCED_FACE('',(#12258),#1715,.F.);
#13207=ADVANCED_FACE('',(#12259),#1716,.F.);
#13208=ADVANCED_FACE('',(#12260,#12261),#317,.T.);
#13209=ADVANCED_FACE('',(#12262,#12263),#318,.T.);
#13210=ADVANCED_FACE('',(#12264,#12265),#319,.T.);
#13211=ADVANCED_FACE('',(#12266,#12267),#320,.T.);
#13518=CLOSED_SHELL('',(#13183,#13184,#13185,#13186,#13187,#13188,#13189,
#13190,#13191,#13192,#13193,#13194,#13195,#13196,#13197,#13198,#13199,#13200,
#13201,#13202,#13203,#13204,#13205,#13206,#13207,#13208,#13209,#13210,#13211));
#13545=STYLED_ITEM('',(#13572),#13735);
#13572=PRESENTATION_STYLE_ASSIGNMENT((#13599));
#13599=SURFACE_STYLE_USAGE(.BOTH.,#13626);
#13626=SURFACE_SIDE_STYLE('',(#13653));
#13653=SURFACE_STYLE_FILL_AREA(#13680);
#13680=FILL_AREA_STYLE('',(#13707));
#13707=FILL_AREA_STYLE_COLOUR('',#60);
#13735=MANIFOLD_SOLID_BREP('Floating_ring',#13518);
#13763=SHAPE_DEFINITION_REPRESENTATION(#45559,#13791);
#13791=SHAPE_REPRESENTATION('Floating_ring',(#13802),#45481);
#13802=AXIS2_PLACEMENT_3D('',#19109,#15295,#15296);
#14699=AXIS2_PLACEMENT_3D('',#35050,#17571,#17572);
#14700=AXIS2_PLACEMENT_3D('',#35059,#17577,#17578);
#14701=AXIS2_PLACEMENT_3D('',#35060,#17579,#17580);
#14702=AXIS2_PLACEMENT_3D('',#35064,#17582,#17583);
#14703=AXIS2_PLACEMENT_3D('',#35065,#17584,#17585);
#14704=AXIS2_PLACEMENT_3D('',#35071,#17589,#17590);
#14705=AXIS2_PLACEMENT_3D('',#35080,#17595,#17596);
#14706=AXIS2_PLACEMENT_3D('',#35089,#17601,#17602);
#14707=AXIS2_PLACEMENT_3D('',#35090,#17603,#17604);
#14708=AXIS2_PLACEMENT_3D('',#35091,#17605,#17606);
#14709=AXIS2_PLACEMENT_3D('',#35092,#17607,#17608);
#14710=AXIS2_PLACEMENT_3D('',#35101,#17613,#17614);
#14711=AXIS2_PLACEMENT_3D('',#35110,#17619,#17620);
#14712=AXIS2_PLACEMENT_3D('',#35111,#17621,#17622);
#14713=AXIS2_PLACEMENT_3D('',#35112,#17623,#17624);
#14714=AXIS2_PLACEMENT_3D('',#35113,#17625,#17626);
#14715=AXIS2_PLACEMENT_3D('',#35114,#17627,#17628);
#14716=AXIS2_PLACEMENT_3D('',#35116,#17629,#17630);
#14717=AXIS2_PLACEMENT_3D('',#35118,#17631,#17632);
#14718=AXIS2_PLACEMENT_3D('',#35119,#17633,#17634);
#14719=AXIS2_PLACEMENT_3D('',#35121,#17635,#17636);
#14720=AXIS2_PLACEMENT_3D('',#35123,#17637,#17638);
#14721=AXIS2_PLACEMENT_3D('',#35124,#17639,#17640);
#14722=AXIS2_PLACEMENT_3D('',#35126,#17641,#17642);
#14723=AXIS2_PLACEMENT_3D('',#35128,#17643,#17644);
#14724=AXIS2_PLACEMENT_3D('',#35129,#17645,#17646);
#14725=AXIS2_PLACEMENT_3D('',#35131,#17647,#17648);
#14726=AXIS2_PLACEMENT_3D('',#35133,#17649,#17650);
#14727=AXIS2_PLACEMENT_3D('',#35135,#17651,#17652);
#14728=AXIS2_PLACEMENT_3D('',#35136,#17653,#17654);
#14729=AXIS2_PLACEMENT_3D('',#35137,#17655,#17656);
#14730=AXIS2_PLACEMENT_3D('',#35138,#17657,#17658);
#14731=AXIS2_PLACEMENT_3D('',#35140,#17659,#17660);
#14732=AXIS2_PLACEMENT_3D('',#35142,#17661,#17662);
#14733=AXIS2_PLACEMENT_3D('',#35143,#17663,#17664);
#14734=AXIS2_PLACEMENT_3D('',#35145,#17665,#17666);
#14735=AXIS2_PLACEMENT_3D('',#35147,#17667,#17668);
#14736=AXIS2_PLACEMENT_3D('',#35149,#17669,#17670);
#14737=AXIS2_PLACEMENT_3D('',#35150,#17671,#17672);
#14738=AXIS2_PLACEMENT_3D('',#35151,#17673,#17674);
#14739=AXIS2_PLACEMENT_3D('',#35152,#17675,#17676);
#14740=AXIS2_PLACEMENT_3D('',#35154,#17677,#17678);
#14741=AXIS2_PLACEMENT_3D('',#35156,#17679,#17680);
#14742=AXIS2_PLACEMENT_3D('',#35157,#17681,#17682);
#14743=AXIS2_PLACEMENT_3D('',#35159,#17683,#17684);
#14744=AXIS2_PLACEMENT_3D('',#35161,#17685,#17686);
#14745=AXIS2_PLACEMENT_3D('',#35162,#17687,#17688);
#14746=AXIS2_PLACEMENT_3D('',#35164,#17689,#17690);
#14747=AXIS2_PLACEMENT_3D('',#35166,#17691,#17692);
#14748=AXIS2_PLACEMENT_3D('',#35167,#17693,#17694);
#14749=AXIS2_PLACEMENT_3D('',#35168,#17695,#17696);
#14750=AXIS2_PLACEMENT_3D('',#35169,#17697,#17698);
#14751=AXIS2_PLACEMENT_3D('',#35170,#17699,#17700);
#14752=AXIS2_PLACEMENT_3D('',#35171,#17701,#17702);
#14753=AXIS2_PLACEMENT_3D('',#35172,#17703,#17704);
#14754=AXIS2_PLACEMENT_3D('',#35173,#17705,#17706);
#14755=AXIS2_PLACEMENT_3D('',#35174,#17707,#17708);
#14756=AXIS2_PLACEMENT_3D('',#35175,#17709,#17710);
#14757=AXIS2_PLACEMENT_3D('',#35176,#17711,#17712);
#14758=AXIS2_PLACEMENT_3D('',#35177,#17713,#17714);
#14759=AXIS2_PLACEMENT_3D('',#35178,#17715,#17716);
#15295=DIRECTION('',(0.,0.,1.));
#15296=DIRECTION('',(1.,0.,0.));
#17571=DIRECTION('',(0.,1.,0.));
#17572=DIRECTION('',(-1.,0.,0.));
#17573=DIRECTION('',(0.,0.,1.));
#17574=DIRECTION('',(-1.,-7.27196081129478E-15,0.));
#17575=DIRECTION('',(0.,0.,1.));
#17576=DIRECTION('',(-1.,-7.27196081129478E-15,0.));
#17577=DIRECTION('',(0.,0.,1.));
#17578=DIRECTION('',(1.,0.,0.));
#17579=DIRECTION('',(0.,0.,1.));
#17580=DIRECTION('',(-0.5,0.866025403784436,0.));
#17581=DIRECTION('',(0.,0.,1.));
#17582=DIRECTION('',(0.,0.,1.));
#17583=DIRECTION('',(1.,0.,0.));
#17584=DIRECTION('',(0.,-1.,0.));
#17585=DIRECTION('',(1.,0.,0.));
#17586=DIRECTION('',(1.,7.66053886991358E-15,0.));
#17587=DIRECTION('',(0.,0.,1.));
#17588=DIRECTION('',(1.,7.66053886991358E-15,0.));
#17589=DIRECTION('',(-0.866025403784433,-0.50000000000001,0.));
#17590=DIRECTION('',(0.50000000000001,-0.866025403784433,0.));
#17591=DIRECTION('',(0.,0.,1.));
#17592=DIRECTION('',(0.50000000000001,-0.866025403784433,0.));
#17593=DIRECTION('',(0.,0.,1.));
#17594=DIRECTION('',(0.50000000000001,-0.866025403784433,0.));
#17595=DIRECTION('',(0.866025403784433,0.500000000000011,0.));
#17596=DIRECTION('',(-0.500000000000011,0.866025403784433,0.));
#17597=DIRECTION('',(0.,0.,1.));
#17598=DIRECTION('',(-0.500000000000011,0.866025403784433,0.));
#17599=DIRECTION('',(0.,0.,1.));
#17600=DIRECTION('',(-0.500000000000011,0.866025403784433,0.));
#17601=DIRECTION('',(0.,0.,1.));
#17602=DIRECTION('',(1.,0.,0.));
#17603=DIRECTION('',(0.,0.,1.));
#17604=DIRECTION('',(-0.499999999999993,-0.866025403784443,0.));
#17605=DIRECTION('',(0.,0.,1.));
#17606=DIRECTION('',(1.,0.,0.));
#17607=DIRECTION('',(0.86602540378444,-0.5,0.));
#17608=DIRECTION('',(0.5,0.86602540378444,0.));
#17609=DIRECTION('',(0.,0.,1.));
#17610=DIRECTION('',(0.5,0.86602540378444,0.));
#17611=DIRECTION('',(0.,0.,1.));
#17612=DIRECTION('',(0.5,0.86602540378444,0.));
#17613=DIRECTION('',(-0.86602540378444,0.5,0.));
#17614=DIRECTION('',(-0.5,-0.86602540378444,0.));
#17615=DIRECTION('',(0.,0.,1.));
#17616=DIRECTION('',(-0.5,-0.86602540378444,0.));
#17617=DIRECTION('',(0.,0.,1.));
#17618=DIRECTION('',(-0.5,-0.86602540378444,0.));
#17619=DIRECTION('',(0.,0.,1.));
#17620=DIRECTION('',(1.,0.,0.));
#17621=DIRECTION('',(0.,0.,1.));
#17622=DIRECTION('',(1.,0.,0.));
#17623=DIRECTION('',(0.,0.,1.));
#17624=DIRECTION('',(1.,0.,0.));
#17625=DIRECTION('',(0.,0.,-1.));
#17626=DIRECTION('',(-1.,0.,0.));
#17627=DIRECTION('',(0.,0.,1.));
#17628=DIRECTION('',(1.,0.,0.));
#17629=DIRECTION('',(0.,0.,1.));
#17630=DIRECTION('',(1.,0.,0.));
#17631=DIRECTION('',(0.,0.,-1.));
#17632=DIRECTION('',(-1.,0.,0.));
#17633=DIRECTION('',(0.,0.,1.));
#17634=DIRECTION('',(1.,0.,0.));
#17635=DIRECTION('',(0.,0.,1.));
#17636=DIRECTION('',(1.,0.,0.));
#17637=DIRECTION('',(0.,0.,-1.));
#17638=DIRECTION('',(-1.,0.,0.));
#17639=DIRECTION('',(0.,0.,1.));
#17640=DIRECTION('',(1.,0.,0.));
#17641=DIRECTION('',(0.,0.,1.));
#17642=DIRECTION('',(1.,0.,0.));
#17643=DIRECTION('',(0.,0.,1.));
#17644=DIRECTION('',(1.,0.,0.));
#17645=DIRECTION('',(0.,0.,1.));
#17646=DIRECTION('',(1.,0.,0.));
#17647=DIRECTION('',(0.,0.,1.));
#17648=DIRECTION('',(1.,0.,0.));
#17649=DIRECTION('',(0.,0.,1.));
#17650=DIRECTION('',(1.,0.,0.));
#17651=DIRECTION('',(0.,0.,1.));
#17652=DIRECTION('',(1.,0.,0.));
#17653=DIRECTION('',(0.,0.,1.));
#17654=DIRECTION('',(-0.499999999999993,-0.866025403784443,0.));
#17655=DIRECTION('',(0.,0.,1.));
#17656=DIRECTION('',(-0.5,0.866025403784436,0.));
#17657=DIRECTION('',(0.,0.,-1.));
#17658=DIRECTION('',(1.,0.,0.));
#17659=DIRECTION('',(0.,0.,1.));
#17660=DIRECTION('',(1.,0.,0.));
#17661=DIRECTION('',(0.,0.,1.));
#17662=DIRECTION('',(1.,0.,0.));
#17663=DIRECTION('',(0.,0.,1.));
#17664=DIRECTION('',(1.,0.,0.));
#17665=DIRECTION('',(0.,0.,1.));
#17666=DIRECTION('',(1.,0.,0.));
#17667=DIRECTION('',(0.,0.,1.));
#17668=DIRECTION('',(1.,0.,0.));
#17669=DIRECTION('',(0.,0.,1.));
#17670=DIRECTION('',(1.,0.,0.));
#17671=DIRECTION('',(0.,0.,1.));
#17672=DIRECTION('',(1.,0.,0.));
#17673=DIRECTION('',(0.,0.,1.));
#17674=DIRECTION('',(1.,0.,0.));
#17675=DIRECTION('',(0.,0.,-1.));
#17676=DIRECTION('',(1.,0.,0.));
#17677=DIRECTION('',(0.,0.,1.));
#17678=DIRECTION('',(1.,0.,0.));
#17679=DIRECTION('',(0.,0.,1.));
#17680=DIRECTION('',(1.,0.,0.));
#17681=DIRECTION('',(0.,0.,-1.));
#17682=DIRECTION('',(1.,0.,0.));
#17683=DIRECTION('',(0.,0.,1.));
#17684=DIRECTION('',(1.,0.,0.));
#17685=DIRECTION('',(0.,0.,1.));
#17686=DIRECTION('',(1.,0.,0.));
#17687=DIRECTION('',(0.,0.,1.));
#17688=DIRECTION('',(1.,0.,0.));
#17689=DIRECTION('',(0.,0.,-1.));
#17690=DIRECTION('',(1.,0.,0.));
#17691=DIRECTION('',(0.,0.,1.));
#17692=DIRECTION('',(1.,0.,0.));
#17693=DIRECTION('',(0.,0.,1.));
#17694=DIRECTION('',(1.,0.,0.));
#17695=DIRECTION('',(0.,0.,1.));
#17696=DIRECTION('',(1.,0.,0.));
#17697=DIRECTION('',(0.,0.,1.));
#17698=DIRECTION('',(1.,0.,0.));
#17699=DIRECTION('',(0.,0.,1.));
#17700=DIRECTION('',(1.,0.,0.));
#17701=DIRECTION('',(0.,0.,1.));
#17702=DIRECTION('',(1.,0.,0.));
#17703=DIRECTION('',(0.,0.,1.));
#17704=DIRECTION('',(1.,0.,0.));
#17705=DIRECTION('',(0.,0.,1.));
#17706=DIRECTION('',(1.,0.,0.));
#17707=DIRECTION('',(0.,0.,1.));
#17708=DIRECTION('',(1.,0.,0.));
#17709=DIRECTION('',(0.,0.,1.));
#17710=DIRECTION('',(1.,0.,0.));
#17711=DIRECTION('',(0.,0.,1.));
#17712=DIRECTION('',(1.,0.,0.));
#17713=DIRECTION('',(0.,0.,1.));
#17714=DIRECTION('',(1.,0.,0.));
#17715=DIRECTION('',(0.,0.,1.));
#17716=DIRECTION('',(1.,0.,0.));
#19109=CARTESIAN_POINT('',(0.,0.,0.));
#35050=CARTESIAN_POINT('',(0.00350000000000028,-0.037,0.092));
#35051=CARTESIAN_POINT('',(0.00350000000000028,-0.037,0.092));
#35052=CARTESIAN_POINT('',(0.00350000000000027,-0.037,0.1));
#35053=CARTESIAN_POINT('',(0.00350000000000027,-0.037,0.103));
#35054=CARTESIAN_POINT('',(0.00350000000000028,-0.037,0.103));
#35055=CARTESIAN_POINT('',(-0.00349999999999974,-0.037,0.103));
#35056=CARTESIAN_POINT('',(-0.00349999999999974,-0.037,0.092));
#35057=CARTESIAN_POINT('',(-0.00349999999999974,-0.037,0.1));
#35058=CARTESIAN_POINT('',(2.69062550017907E-16,-0.037,0.1));
#35059=CARTESIAN_POINT('',(-0.00349999999999973,-0.038,0.092));
#35060=CARTESIAN_POINT('',(-0.00349999999999973,-0.038,0.103));
#35061=CARTESIAN_POINT('',(-0.00349999999999972,-0.039,0.103));
#35062=CARTESIAN_POINT('',(-0.00349999999999972,-0.039,0.092));
#35063=CARTESIAN_POINT('',(-0.00349999999999972,-0.039,0.1));
#35064=CARTESIAN_POINT('',(-0.00349999999999973,-0.038,0.1));
#35065=CARTESIAN_POINT('',(0.00350000000000029,-0.039,0.092));
#35066=CARTESIAN_POINT('',(0.00350000000000029,-0.039,0.103));
#35067=CARTESIAN_POINT('',(0.00350000000000029,-0.039,0.103));
#35068=CARTESIAN_POINT('',(0.00350000000000029,-0.039,0.092));
#35069=CARTESIAN_POINT('',(0.00350000000000029,-0.039,0.1));
#35070=CARTESIAN_POINT('',(2.9876101592663E-16,-0.039,0.1));
#35071=CARTESIAN_POINT('',(0.030292939940024,0.0215310889132459,0.092));
#35072=CARTESIAN_POINT('',(0.030292939940024,0.0215310889132459,0.092));
#35073=CARTESIAN_POINT('',(0.030292939940024,0.0215310889132459,0.1));
#35074=CARTESIAN_POINT('',(0.030292939940024,0.0215310889132459,0.103));
#35075=CARTESIAN_POINT('',(0.030292939940024,0.0215310889132459,0.103));
#35076=CARTESIAN_POINT('',(0.033792939940024,0.0154689110867548,0.103));
#35077=CARTESIAN_POINT('',(0.033792939940024,0.0154689110867548,0.092));
#35078=CARTESIAN_POINT('',(0.033792939940024,0.0154689110867548,0.1));
#35079=CARTESIAN_POINT('',(0.032042939940024,0.0185000000000004,0.1));
#35080=CARTESIAN_POINT('',(0.0320249907475929,0.0225310889132459,0.092));
#35081=CARTESIAN_POINT('',(0.0355249907475929,0.0164689110867549,0.092));
#35082=CARTESIAN_POINT('',(0.0355249907475929,0.0164689110867549,0.1));
#35083=CARTESIAN_POINT('',(0.0355249907475929,0.0164689110867549,0.103));
#35084=CARTESIAN_POINT('',(0.0320249907475929,0.0225310889132459,0.103));
#35085=CARTESIAN_POINT('',(0.0320249907475929,0.0225310889132459,0.103));
#35086=CARTESIAN_POINT('',(0.0320249907475929,0.0225310889132459,0.092));
#35087=CARTESIAN_POINT('',(0.0320249907475929,0.0225310889132459,0.1));
#35088=CARTESIAN_POINT('',(0.0337749907475929,0.0195000000000004,0.1));
#35089=CARTESIAN_POINT('',(0.0311589653438084,0.0220310889132459,0.092));
#35090=CARTESIAN_POINT('',(0.0311589653438084,0.0220310889132459,0.103));
#35091=CARTESIAN_POINT('',(0.0311589653438084,0.0220310889132459,0.1));
#35092=CARTESIAN_POINT('',(-0.0337929399400243,0.0154689110867544,0.092));
#35093=CARTESIAN_POINT('',(-0.0337929399400243,0.0154689110867544,0.092));
#35094=CARTESIAN_POINT('',(-0.0337929399400243,0.0154689110867544,0.1));
#35095=CARTESIAN_POINT('',(-0.0337929399400243,0.0154689110867544,0.103));
#35096=CARTESIAN_POINT('',(-0.0337929399400243,0.0154689110867544,0.103));
#35097=CARTESIAN_POINT('',(-0.0302929399400243,0.0215310889132454,0.103));
#35098=CARTESIAN_POINT('',(-0.0302929399400243,0.0215310889132454,0.092));
#35099=CARTESIAN_POINT('',(-0.0302929399400243,0.0215310889132454,0.1));
#35100=CARTESIAN_POINT('',(-0.0320429399400243,0.0185,0.1));
#35101=CARTESIAN_POINT('',(-0.0355249907475932,0.0164689110867543,0.092));
#35102=CARTESIAN_POINT('',(-0.0320249907475932,0.0225310889132454,0.092));
#35103=CARTESIAN_POINT('',(-0.0320249907475932,0.0225310889132454,0.1));
#35104=CARTESIAN_POINT('',(-0.0320249907475932,0.0225310889132454,0.103));
#35105=CARTESIAN_POINT('',(-0.0355249907475932,0.0164689110867543,0.103));
#35106=CARTESIAN_POINT('',(-0.0355249907475932,0.0164689110867543,0.103));
#35107=CARTESIAN_POINT('',(-0.0355249907475932,0.0164689110867543,0.092));
#35108=CARTESIAN_POINT('',(-0.0355249907475932,0.0164689110867543,0.1));
#35109=CARTESIAN_POINT('',(-0.0337749907475932,0.0195,0.1));
#35110=CARTESIAN_POINT('',(-0.0346589653438087,0.0159689110867543,0.092));
#35111=CARTESIAN_POINT('',(-0.0346589653438087,0.0159689110867543,0.103));
#35112=CARTESIAN_POINT('',(-0.0346589653438087,0.0159689110867543,0.1));
#35113=CARTESIAN_POINT('',(-0.024761562113538,-0.0149999999999972,0.10173));
#35114=CARTESIAN_POINT('',(0.,0.03,0.10173));
#35115=CARTESIAN_POINT('',(0.00277876,0.03,0.10173));
#35116=CARTESIAN_POINT('',(0.,0.03,0.10173));
#35117=CARTESIAN_POINT('',(0.0012192,0.03,0.10173));
#35118=CARTESIAN_POINT('',(-0.024761562113538,-0.0149999999999972,0.10173));
#35119=CARTESIAN_POINT('',(-0.025980762113538,-0.0149999999999972,0.10173));
#35120=CARTESIAN_POINT('',(-0.023202002113538,-0.0149999999999972,0.10173));
#35121=CARTESIAN_POINT('',(-0.025980762113538,-0.0149999999999972,0.10173));
#35122=CARTESIAN_POINT('',(-0.024761562113538,-0.0149999999999972,0.10173));
#35123=CARTESIAN_POINT('',(-0.024761562113538,-0.0149999999999972,0.10173));
#35124=CARTESIAN_POINT('',(0.0259807621135283,-0.0150000000000028,0.10173));
#35125=CARTESIAN_POINT('',(0.0287595221135283,-0.0150000000000028,0.10173));
#35126=CARTESIAN_POINT('',(0.0259807621135283,-0.0150000000000028,0.10173));
#35127=CARTESIAN_POINT('',(0.0271999621135283,-0.0150000000000028,0.10173));
#35128=CARTESIAN_POINT('',(0.,0.,0.103));
#35129=CARTESIAN_POINT('',(0.0259807621135283,-0.0150000000000028,0.103));
#35130=CARTESIAN_POINT('',(0.0287595221135283,-0.0150000000000028,0.103));
#35131=CARTESIAN_POINT('',(-0.025980762113538,-0.0149999999999972,0.103));
#35132=CARTESIAN_POINT('',(-0.023202002113538,-0.0149999999999972,0.103));
#35133=CARTESIAN_POINT('',(0.,0.03,0.103));
#35134=CARTESIAN_POINT('',(0.00277876,0.03,0.103));
#35135=CARTESIAN_POINT('',(-0.0311589653438087,0.0220310889132454,0.103));
#35136=CARTESIAN_POINT('',(0.0346589653438085,0.0159689110867548,0.103));
#35137=CARTESIAN_POINT('',(0.00350000000000028,-0.038,0.103));
#35138=CARTESIAN_POINT('',(0.,0.,0.103));
#35139=CARTESIAN_POINT('',(0.0104331778036387,0.,0.103));
#35140=CARTESIAN_POINT('',(0.,0.,0.103));
#35141=CARTESIAN_POINT('',(0.044,0.,0.103));
#35142=CARTESIAN_POINT('',(0.,0.,0.1));
#35143=CARTESIAN_POINT('',(0.0259807621135283,-0.0150000000000028,0.1));
#35144=CARTESIAN_POINT('',(0.0271999621135283,-0.0150000000000028,0.1));
#35145=CARTESIAN_POINT('',(-0.025980762113538,-0.0149999999999972,0.1));
#35146=CARTESIAN_POINT('',(-0.024761562113538,-0.0149999999999972,0.1));
#35147=CARTESIAN_POINT('',(0.,0.03,0.1));
#35148=CARTESIAN_POINT('',(0.0012192,0.03,0.1));
#35149=CARTESIAN_POINT('',(-0.0311589653438087,0.0220310889132454,0.1));
#35150=CARTESIAN_POINT('',(0.0346589653438085,0.0159689110867548,0.1));
#35151=CARTESIAN_POINT('',(0.00350000000000028,-0.038,0.1));
#35152=CARTESIAN_POINT('',(0.,0.,0.1));
#35153=CARTESIAN_POINT('',(0.044,0.,0.1));
#35154=CARTESIAN_POINT('',(0.,0.,0.1));
#35155=CARTESIAN_POINT('',(0.0104331778036387,0.,0.1));
#35156=CARTESIAN_POINT('',(0.,0.,0.1));
#35157=CARTESIAN_POINT('',(0.,0.,0.102));
#35158=CARTESIAN_POINT('',(0.045,0.,0.102));
#35159=CARTESIAN_POINT('',(0.,0.,0.101));
#35160=CARTESIAN_POINT('',(0.045,0.,0.101));
#35161=CARTESIAN_POINT('',(0.,0.,0.083));
#35162=CARTESIAN_POINT('',(0.,0.,0.102));
#35163=CARTESIAN_POINT('',(0.00943317780363869,0.,0.102));
#35164=CARTESIAN_POINT('',(0.,0.,0.101));
#35165=CARTESIAN_POINT('',(0.00943317780363869,0.,0.101));
#35166=CARTESIAN_POINT('',(0.0259807621135283,-0.0150000000000028,0.103));
#35167=CARTESIAN_POINT('',(0.0259807621135283,-0.0150000000000028,0.103));
#35168=CARTESIAN_POINT('',(-0.025980762113538,-0.0149999999999972,0.103));
#35169=CARTESIAN_POINT('',(-0.025980762113538,-0.0149999999999972,0.103));
#35170=CARTESIAN_POINT('',(0.,0.03,0.103));
#35171=CARTESIAN_POINT('',(0.,0.03,0.103));
#35172=CARTESIAN_POINT('',(-0.0311589653438087,0.0220310889132454,0.092));
#35173=CARTESIAN_POINT('',(0.0346589653438085,0.0159689110867548,0.092));
#35174=CARTESIAN_POINT('',(0.00350000000000028,-0.038,0.092));
#35175=CARTESIAN_POINT('',(0.,0.,0.101));
#35176=CARTESIAN_POINT('',(0.,0.,0.101));
#35177=CARTESIAN_POINT('',(0.,0.,0.102));
#35178=CARTESIAN_POINT('',(0.,0.,0.102));
#45463=MECHANICAL_DESIGN_GEOMETRIC_PRESENTATION_REPRESENTATION('',(#13545),#45464);
#45464=(
GEOMETRIC_REPRESENTATION_CONTEXT(3)
GLOBAL_UNCERTAINTY_ASSIGNED_CONTEXT((#45492))
GLOBAL_UNIT_ASSIGNED_CONTEXT((#45522,#45521,#45520))
REPRESENTATION_CONTEXT('MAS-690','TOP_LEVEL_ASSEMBLY_PART')
);
#45481=(
GEOMETRIC_REPRESENTATION_CONTEXT(3)
GLOBAL_UNCERTAINTY_ASSIGNED_CONTEXT((#45509))
GLOBAL_UNIT_ASSIGNED_CONTEXT((#45522,#45521,#45520))
REPRESENTATION_CONTEXT('Floating_ring','COMPONENT_PART')
);
#45492=UNCERTAINTY_MEASURE_WITH_UNIT(LENGTH_MEASURE(1.E-8),#45522,
'DISTANCE_ACCURACY_VALUE','Maximum Tolerance applied to model');
#45509=UNCERTAINTY_MEASURE_WITH_UNIT(LENGTH_MEASURE(1.E-6),#45522,
'DISTANCE_ACCURACY_VALUE','Maximum Tolerance applied to model');
#45520=(
NAMED_UNIT(*)
SI_UNIT($,.STERADIAN.)
SOLID_ANGLE_UNIT()
);
#45521=(
NAMED_UNIT(*)
PLANE_ANGLE_UNIT()
SI_UNIT($,.RADIAN.)
);
#45522=(
LENGTH_UNIT()
NAMED_UNIT(*)
SI_UNIT($,.METRE.)
);
#45559=PRODUCT_DEFINITION_SHAPE('','',#45602);
#45602=PRODUCT_DEFINITION('','',#45658,#45630);
#45630=PRODUCT_DEFINITION_CONTEXT('',#45782,'design');
#45658=PRODUCT_DEFINITION_FORMATION_WITH_SPECIFIED_SOURCE('','',#45714,
 .NOT_KNOWN.);
#45714=PRODUCT('Floating_ring','Floating_ring','Floating_ring',(#45770));
#45770=PRODUCT_CONTEXT('',#45782,'mechanical');
#45782=APPLICATION_CONTEXT('managed model based 3d engineering');
ENDSEC;
END-ISO-10303-21;
